ISO-10303-21;
HEADER;
FILE_DESCRIPTION (('STEP AP214'),
    '1' );
FILE_NAME ('Part 136_Varsay\X2\0131\X0\lan.step',
    '2026-10-08T11:03:28',
    ( '' ),
    ( '' ),
    'SwSTEP 2.0',
    'SolidWorks 2024',
    '' );
FILE_SCHEMA (( 'AUTOMOTIVE_DESIGN' ));
ENDSEC;

DATA;
#14=PRODUCT_DEFINITION ( 'UNKNOWN', '', #194, #518 ) ;
#35=CARTESIAN_POINT ( 'NONE',  ( 3.749999999999999556, 3.750000000000000000, 3.749999999999995559 ) ) ;
#43=PLANE ( 'NONE',  #271 ) ;
#44=VERTEX_POINT ( 'NONE', #445 ) ;
#59=EDGE_CURVE ( 'NONE', #4262, #44, #387, .T. ) ;
#65=FACE_OUTER_BOUND ( 'NONE', #1668, .T. ) ;
#77=ORIENTED_EDGE ( 'NONE', *, *, #3651, .T. ) ;
#103=EDGE_LOOP ( 'NONE', ( #548, #3228, #3814, #302 ) ) ;
#107=DIRECTION ( 'NONE',  ( 0.000000000000000000, 0.000000000000000000, 1.000000000000000000 ) ) ;
#112=DIRECTION ( 'NONE',  ( -8.673617379884035472E-17, 1.000000000000000000, -0.000000000000000000 ) ) ;
#129=DIRECTION ( 'NONE',  ( 0.000000000000000000, 0.000000000000000000, 1.000000000000000000 ) ) ;
#130=DIRECTION ( 'NONE',  ( -0.000000000000000000, -0.000000000000000000, -1.000000000000000000 ) ) ;
#145=ORIENTED_EDGE ( 'NONE', *, *, #329, .T. ) ;
#152=DIRECTION ( 'NONE',  ( 8.673617379884035472E-17, 1.000000000000000000, 0.000000000000000000 ) ) ;
#154=VECTOR ( 'NONE', #4373, 1000.000000000000000 ) ;
#170=CARTESIAN_POINT ( 'NONE',  ( -3.749999999999999556, -3.750000000000000888, 131.2499999999999716 ) ) ;
#171=ORIENTED_EDGE ( 'NONE', *, *, #591, .T. ) ;
#194=PRODUCT_DEFINITION_FORMATION_WITH_SPECIFIED_SOURCE ( 'ANY', '', #1335, .NOT_KNOWN. ) ;
#199=UNCERTAINTY_MEASURE_WITH_UNIT (LENGTH_MEASURE( 1.000000000000000082E-05 ), #312, 'distance_accuracy_value', 'NONE');
#244=PRESENTATION_STYLE_ASSIGNMENT (( #4572 ) ) ;
#259=EDGE_CURVE ( 'NONE', #359, #3792, #1269, .T. ) ;
#266=DIRECTION ( 'NONE',  ( 8.673617379884035472E-17, 1.000000000000000000, -0.000000000000000000 ) ) ;
#271=AXIS2_PLACEMENT_3D ( 'NONE', #3619, #4325, #2577 ) ;
#274=FACE_OUTER_BOUND ( 'NONE', #558, .T. ) ;
#275=MANIFOLD_SOLID_BREP ( 'Ölçek1', #1022 ) ;
#283=AXIS2_PLACEMENT_3D ( 'NONE', #969, #1010, #610 ) ;
#284=CARTESIAN_POINT ( 'NONE',  ( -3.750000000000000000, 3.750000000000000000, 18.74999999999999645 ) ) ;
#298=CARTESIAN_POINT ( 'NONE',  ( -3.750000000000000888, -3.750000000000000000, 3.749999999999995559 ) ) ;
#299=DIRECTION ( 'NONE',  ( 0.000000000000000000, 0.000000000000000000, 1.000000000000000000 ) ) ;
#302=ORIENTED_EDGE ( 'NONE', *, *, #1589, .T. ) ;
#303=EDGE_CURVE ( 'NONE', #1254, #359, #4238, .T. ) ;
#305=AXIS2_PLACEMENT_3D ( 'NONE', #1975, #3706, #3407 ) ;
#311=AXIS2_PLACEMENT_3D ( 'NONE', #4250, #3824, #4584 ) ;
#312=( LENGTH_UNIT ( ) NAMED_UNIT ( * ) SI_UNIT ( .MILLI., .METRE. ) );
#326=CARTESIAN_POINT ( 'NONE',  ( 3.750000000000000888, -3.750000000000000000, 131.2499999999999716 ) ) ;
#329=EDGE_CURVE ( 'NONE', #1870, #4530, #4549, .T. ) ;
#333=CARTESIAN_POINT ( 'NONE',  ( 14.28750000000000142, 1.746464731918909201E-15, 18.74999999999999645 ) ) ;
#353=DIRECTION ( 'NONE',  ( -1.000000000000000000, 0.000000000000000000, 0.000000000000000000 ) ) ;
#359=VERTEX_POINT ( 'NONE', #284 ) ;
#376=FACE_BOUND ( 'NONE', #1894, .T. ) ;
#384=CIRCLE ( 'NONE', #756, 14.28750000000000142 ) ;
#387=LINE ( 'NONE', #3242, #464 ) ;
#394=DIRECTION ( 'NONE',  ( 1.000000000000000000, 0.000000000000000000, 0.000000000000000000 ) ) ;
#401=EDGE_CURVE ( 'NONE', #2368, #1254, #2888, .T. ) ;
#412=CARTESIAN_POINT ( 'NONE',  ( 3.750000000000000888, -3.750000000000000000, 131.2499999999999716 ) ) ;
#437=CARTESIAN_POINT ( 'NONE',  ( -9.549434556529077899E-17, -3.249382362871961689E-18, 18.74999999999999645 ) ) ;
#445=CARTESIAN_POINT ( 'NONE',  ( 3.749999999999999556, -3.750000000000000888, 3.749999999999995559 ) ) ;
#448=EDGE_CURVE ( 'NONE', #4520, #4090, #3716, .T. ) ;
#449=ORIENTED_EDGE ( 'NONE', *, *, #526, .F. ) ;
#455=FACE_OUTER_BOUND ( 'NONE', #868, .T. ) ;
#464=VECTOR ( 'NONE', #3232, 1000.000000000000000 ) ;
#469=CARTESIAN_POINT ( 'NONE',  ( 3.750000000000000000, 3.750000000000000000, 131.2499999999999716 ) ) ;
#492=DIRECTION ( 'NONE',  ( -1.000000000000000000, -0.000000000000000000, -0.000000000000000000 ) ) ;
#494=ORIENTED_EDGE ( 'NONE', *, *, #3566, .F. ) ;
#501=VERTEX_POINT ( 'NONE', #2658 ) ;
#518=PRODUCT_DEFINITION_CONTEXT ( 'detailed design', #2244, 'design' ) ;
#526=EDGE_CURVE ( 'NONE', #501, #1254, #2610, .T. ) ;
#528=AXIS2_PLACEMENT_3D ( 'NONE', #3551, #299, #1006 ) ;
#534=FACE_OUTER_BOUND ( 'NONE', #2535, .T. ) ;
#547=EDGE_CURVE ( 'NONE', #4090, #3312, #3392, .T. ) ;
#548=ORIENTED_EDGE ( 'NONE', *, *, #2840, .T. ) ;
#558=EDGE_LOOP ( 'NONE', ( #3534, #1921, #2456, #145 ) ) ;
#571=LINE ( 'NONE', #3818, #3067 ) ;
#589=ORIENTED_EDGE ( 'NONE', *, *, #3566, .T. ) ;
#591=EDGE_CURVE ( 'NONE', #2688, #3887, #2455, .T. ) ;
#595=DIRECTION ( 'NONE',  ( 1.000000000000000000, 8.673617379884035472E-17, -0.000000000000000000 ) ) ;
#604=ORIENTED_EDGE ( 'NONE', *, *, #1834, .F. ) ;
#610=DIRECTION ( 'NONE',  ( 1.000000000000000000, 0.000000000000000000, -0.000000000000000000 ) ) ;
#627=ORIENTED_EDGE ( 'NONE', *, *, #591, .F. ) ;
#630=ORIENTED_EDGE ( 'NONE', *, *, #59, .F. ) ;
#634=ORIENTED_EDGE ( 'NONE', *, *, #547, .F. ) ;
#646=CARTESIAN_POINT ( 'NONE',  ( -3.749999999999999556, -3.750000000000000888, 146.2500000000000000 ) ) ;
#648=DIRECTION ( 'NONE',  ( 1.000000000000000000, 0.000000000000000000, 0.000000000000000000 ) ) ;
#683=AXIS2_PLACEMENT_3D ( 'NONE', #882, #3332, #1973 ) ;
#685=ORIENTED_EDGE ( 'NONE', *, *, #526, .T. ) ;
#690=DIRECTION ( 'NONE',  ( -0.000000000000000000, -1.000000000000000000, -0.000000000000000000 ) ) ;
#700=FACE_OUTER_BOUND ( 'NONE', #2771, .T. ) ;
#701=ORIENTED_EDGE ( 'NONE', *, *, #3222, .T. ) ;
#726=VECTOR ( 'NONE', #2088, 1000.000000000000000 ) ;
#744=VERTEX_POINT ( 'NONE', #1184 ) ;
#756=AXIS2_PLACEMENT_3D ( 'NONE', #1719, #3434, #648 ) ;
#771=CARTESIAN_POINT ( 'NONE',  ( 3.749999999999999556, -3.750000000000000888, 3.749999999999995559 ) ) ;
#783=DIRECTION ( 'NONE',  ( 1.000000000000000000, 0.000000000000000000, -0.000000000000000000 ) ) ;
#788=ORIENTED_EDGE ( 'NONE', *, *, #1129, .F. ) ;
#792=EDGE_CURVE ( 'NONE', #4332, #744, #3761, .T. ) ;
#817=DIRECTION ( 'NONE',  ( 1.000000000000000000, 0.000000000000000000, -0.000000000000000000 ) ) ;
#828=EDGE_CURVE ( 'NONE', #744, #2975, #2549, .T. ) ;
#834=DIRECTION ( 'NONE',  ( 0.000000000000000000, 0.000000000000000000, -1.000000000000000000 ) ) ;
#854=ADVANCED_FACE ( 'NONE', ( #2156 ), #4440, .F. ) ;
#856=ORIENTED_EDGE ( 'NONE', *, *, #3651, .F. ) ;
#861=DIRECTION ( 'NONE',  ( 1.000000000000000000, 0.000000000000000000, 0.000000000000000000 ) ) ;
#868=EDGE_LOOP ( 'NONE', ( #3791, #1806, #856, #2282 ) ) ;
#882=CARTESIAN_POINT ( 'NONE',  ( -9.549434556529077899E-17, -3.249382362871961689E-18, 146.2500000000000000 ) ) ;
#890=CARTESIAN_POINT ( 'NONE',  ( 3.749999999999999556, 3.750000000000000000, 3.749999999999995559 ) ) ;
#893=ADVANCED_FACE ( 'NONE', ( #534 ), #4490, .F. ) ;
#894=EDGE_CURVE ( 'NONE', #2688, #4520, #1274, .T. ) ;
#950=ADVANCED_FACE ( 'NONE', ( #2758 ), #2378, .T. ) ;
#956=( NAMED_UNIT ( * ) PLANE_ANGLE_UNIT ( ) SI_UNIT ( $, .RADIAN. ) );
#969=CARTESIAN_POINT ( 'NONE',  ( -9.549434556529077899E-17, -3.249382362871961689E-18, 3.749999999999995559 ) ) ;
#978=DIRECTION ( 'NONE',  ( -0.000000000000000000, -0.000000000000000000, -1.000000000000000000 ) ) ;
#1004=CARTESIAN_POINT ( 'NONE',  ( -14.28750000000000142, -3.249382362871961689E-18, 131.2499999999999716 ) ) ;
#1006=DIRECTION ( 'NONE',  ( 1.000000000000000000, 0.000000000000000000, 0.000000000000000000 ) ) ;
#1010=DIRECTION ( 'NONE',  ( 0.000000000000000000, 0.000000000000000000, 1.000000000000000000 ) ) ;
#1014=EDGE_LOOP ( 'NONE', ( #2060, #2291, #2313, #4100 ) ) ;
#1017=( NAMED_UNIT ( * ) SI_UNIT ( $, .STERADIAN. ) SOLID_ANGLE_UNIT ( ) );
#1022=CLOSED_SHELL ( 'NONE', ( #2136, #1105, #1564, #950, #893, #3020, #1395, #854, #3469, #3039, #3338, #4640, #2519, #3985 ) ) ;
#1024=( NAMED_UNIT ( * ) SI_UNIT ( $, .STERADIAN. ) SOLID_ANGLE_UNIT ( ) );
#1026=DIRECTION ( 'NONE',  ( -1.000000000000000000, 0.000000000000000000, 0.000000000000000000 ) ) ;
#1028=CIRCLE ( 'NONE', #1643, 14.28750000000000142 ) ;
#1040=ORIENTED_EDGE ( 'NONE', *, *, #3222, .F. ) ;
#1046=ORIENTED_EDGE ( 'NONE', *, *, #1699, .F. ) ;
#1079=LINE ( 'NONE', #35, #4372 ) ;
#1090=ORIENTED_EDGE ( 'NONE', *, *, #401, .T. ) ;
#1105=ADVANCED_FACE ( 'NONE', ( #2603, #376 ), #1819, .F. ) ;
#1129=EDGE_CURVE ( 'NONE', #4530, #4520, #3688, .T. ) ;
#1149=EDGE_LOOP ( 'NONE', ( #3203, #634, #2554, #788 ) ) ;
#1159=CARTESIAN_POINT ( 'NONE',  ( -9.549434556529077899E-17, -3.249382362871961689E-18, 131.2499999999999716 ) ) ;
#1180=CARTESIAN_POINT ( 'NONE',  ( -3.750000000000000000, 3.750000000000000000, 3.749999999999995559 ) ) ;
#1181=CARTESIAN_POINT ( 'NONE',  ( -3.750000000000000000, 3.750000000000000000, 3.749999999999995559 ) ) ;
#1184=CARTESIAN_POINT ( 'NONE',  ( 14.28750000000000142, 1.746464731918909201E-15, 131.2499999999999716 ) ) ;
#1192=CARTESIAN_POINT ( 'NONE',  ( -9.549434556529077899E-17, 3.750000000000000000, 131.2499999999999716 ) ) ;
#1237=STYLED_ITEM ( 'NONE', ( #244 ), #275 ) ;
#1243=FACE_OUTER_BOUND ( 'NONE', #1014, .T. ) ;
#1254=VERTEX_POINT ( 'NONE', #1308 ) ;
#1269=LINE ( 'NONE', #2686, #1421 ) ;
#1274=LINE ( 'NONE', #2693, #2706 ) ;
#1295=LINE ( 'NONE', #3091, #2399 ) ;
#1297=APPLICATION_CONTEXT ( 'automotive_design' ) ;
#1308=CARTESIAN_POINT ( 'NONE',  ( -3.750000000000001776, -3.750000000000000000, 18.74999999999999645 ) ) ;
#1316=EDGE_CURVE ( 'NONE', #3312, #4530, #3527, .T. ) ;
#1335=PRODUCT ( 'Part 136_Varsay\X2\0131\X0\lan', 'Part 136_Varsay\X2\0131\X0\lan', '', ( #2468 ) ) ;
#1344=DIRECTION ( 'NONE',  ( -1.000000000000000000, 8.673617379884035472E-17, 0.000000000000000000 ) ) ;
#1358=ORIENTED_EDGE ( 'NONE', *, *, #3194, .T. ) ;
#1359=CARTESIAN_POINT ( 'NONE',  ( -3.750000000000000000, 3.750000000000000000, 18.74999999999999645 ) ) ;
#1363=DIRECTION ( 'NONE',  ( -0.000000000000000000, -0.000000000000000000, 1.000000000000000000 ) ) ;
#1367=DIRECTION ( 'NONE',  ( -0.000000000000000000, -0.000000000000000000, -1.000000000000000000 ) ) ;
#1376=EDGE_CURVE ( 'NONE', #1428, #2975, #1743, .T. ) ;
#1395=ADVANCED_FACE ( 'NONE', ( #274 ), #4632, .F. ) ;
#1404=ORIENTED_EDGE ( 'NONE', *, *, #448, .T. ) ;
#1417=CARTESIAN_POINT ( 'NONE',  ( 3.750000000000000000, 3.750000000000000000, 146.2500000000000000 ) ) ;
#1421=VECTOR ( 'NONE', #2709, 1000.000000000000000 ) ;
#1428=VERTEX_POINT ( 'NONE', #3828 ) ;
#1444=AXIS2_PLACEMENT_3D ( 'NONE', #4245, #978, #1026 ) ;
#1456=ORIENTED_EDGE ( 'NONE', *, *, #3709, .F. ) ;
#1481=LINE ( 'NONE', #646, #1897 ) ;
#1507=FACE_BOUND ( 'NONE', #1149, .T. ) ;
#1514=CARTESIAN_POINT ( 'NONE',  ( -3.749999999999999556, 3.750000000000000000, 131.2499999999999716 ) ) ;
#1551=FACE_OUTER_BOUND ( 'NONE', #3514, .T. ) ;
#1564=ADVANCED_FACE ( 'NONE', ( #3268, #1507 ), #4371, .T. ) ;
#1566=DIRECTION ( 'NONE',  ( -0.000000000000000000, -0.000000000000000000, 1.000000000000000000 ) ) ;
#1583=AXIS2_PLACEMENT_3D ( 'NONE', #1159, #4013, #783 ) ;
#1589=EDGE_CURVE ( 'NONE', #501, #2642, #4394, .T. ) ;
#1601=PLANE ( 'NONE',  #1782 ) ;
#1614=DIRECTION ( 'NONE',  ( -0.000000000000000000, -1.000000000000000000, -0.000000000000000000 ) ) ;
#1643=AXIS2_PLACEMENT_3D ( 'NONE', #437, #3683, #394 ) ;
#1664=CARTESIAN_POINT ( 'NONE',  ( -3.749999999999999556, 3.750000000000000000, 146.2500000000000000 ) ) ;
#1668=EDGE_LOOP ( 'NONE', ( #3474, #1040, #4467, #3125 ) ) ;
#1677=CARTESIAN_POINT ( 'NONE',  ( 3.749999999999999556, -3.750000000000000888, 18.74999999999999645 ) ) ;
#1687=VECTOR ( 'NONE', #2049, 1000.000000000000000 ) ;
#1698=CARTESIAN_POINT ( 'NONE',  ( 3.750000000000000888, -3.750000000000000000, 146.2500000000000000 ) ) ;
#1699=EDGE_CURVE ( 'NONE', #3887, #4090, #4106, .T. ) ;
#1719=CARTESIAN_POINT ( 'NONE',  ( -9.549434556529077899E-17, -3.249382362871961689E-18, 131.2499999999999716 ) ) ;
#1743=CIRCLE ( 'NONE', #528, 14.28750000000000142 ) ;
#1745=CARTESIAN_POINT ( 'NONE',  ( -3.749999999999999556, -3.750000000000000888, 131.2499999999999716 ) ) ;
#1747=AXIS2_PLACEMENT_3D ( 'NONE', #3292, #107, #2597 ) ;
#1774=ORIENTED_EDGE ( 'NONE', *, *, #4281, .F. ) ;
#1782=AXIS2_PLACEMENT_3D ( 'NONE', #1180, #3378, #152 ) ;
#1793=EDGE_CURVE ( 'NONE', #4332, #1428, #3481, .T. ) ;
#1798=DIRECTION ( 'NONE',  ( 0.000000000000000000, 0.000000000000000000, 1.000000000000000000 ) ) ;
#1806=ORIENTED_EDGE ( 'NONE', *, *, #329, .F. ) ;
#1810=VECTOR ( 'NONE', #130, 1000.000000000000000 ) ;
#1819=PLANE ( 'NONE',  #3250 ) ;
#1834=EDGE_CURVE ( 'NONE', #3792, #2368, #4246, .T. ) ;
#1870=VERTEX_POINT ( 'NONE', #1698 ) ;
#1894=EDGE_LOOP ( 'NONE', ( #604, #2337, #3690, #2763 ) ) ;
#1897=VECTOR ( 'NONE', #690, 1000.000000000000000 ) ;
#1901=CARTESIAN_POINT ( 'NONE',  ( -3.749999999999999556, 3.750000000000000000, 146.2500000000000000 ) ) ;
#1921=ORIENTED_EDGE ( 'NONE', *, *, #894, .F. ) ;
#1929=ORIENTED_EDGE ( 'NONE', *, *, #3279, .T. ) ;
#1944=CARTESIAN_POINT ( 'NONE',  ( -9.549434556529077899E-17, -3.249382362871961689E-18, 131.2499999999999716 ) ) ;
#1959=ORIENTED_EDGE ( 'NONE', *, *, #1793, .T. ) ;
#1973=DIRECTION ( 'NONE',  ( -1.000000000000000000, 0.000000000000000000, -0.000000000000000000 ) ) ;
#1975=CARTESIAN_POINT ( 'NONE',  ( -9.549434556529077899E-17, 3.750000000000000000, 146.2500000000000000 ) ) ;
#2011=EDGE_LOOP ( 'NONE', ( #1090, #449, #4613, #589 ) ) ;
#2017=DIRECTION ( 'NONE',  ( -0.000000000000000000, -0.000000000000000000, -1.000000000000000000 ) ) ;
#2023=FACE_OUTER_BOUND ( 'NONE', #2011, .T. ) ;
#2049=DIRECTION ( 'NONE',  ( 1.000000000000000000, 8.673617379884035472E-17, -0.000000000000000000 ) ) ;
#2057=VECTOR ( 'NONE', #4529, 1000.000000000000000 ) ;
#2059=( NAMED_UNIT ( * ) PLANE_ANGLE_UNIT ( ) SI_UNIT ( $, .RADIAN. ) );
#2060=ORIENTED_EDGE ( 'NONE', *, *, #3279, .F. ) ;
#2088=DIRECTION ( 'NONE',  ( -0.000000000000000000, -0.000000000000000000, 1.000000000000000000 ) ) ;
#2109=LINE ( 'NONE', #3124, #726 ) ;
#2110=AXIS2_PLACEMENT_3D ( 'NONE', #2289, #861, #834 ) ;
#2112=DIRECTION ( 'NONE',  ( -1.000000000000000000, -0.000000000000000000, -0.000000000000000000 ) ) ;
#2136=ADVANCED_FACE ( 'NONE', ( #1243 ), #3747, .T. ) ;
#2139=PLANE ( 'NONE',  #3558 ) ;
#2156=FACE_OUTER_BOUND ( 'NONE', #4381, .T. ) ;
#2162=CARTESIAN_POINT ( 'NONE',  ( 3.750000000000000888, -3.750000000000000000, 146.2500000000000000 ) ) ;
#2193=EDGE_LOOP ( 'NONE', ( #2582, #1929 ) ) ;
#2201=MECHANICAL_DESIGN_GEOMETRIC_PRESENTATION_REPRESENTATION('',(#1237),#4080);
#2213=EDGE_LOOP ( 'NONE', ( #2250, #3855 ) ) ;
#2244=APPLICATION_CONTEXT ( 'automotive_design' ) ;
#2250=ORIENTED_EDGE ( 'NONE', *, *, #1376, .F. ) ;
#2271=DIRECTION ( 'NONE',  ( -0.000000000000000000, -0.000000000000000000, -1.000000000000000000 ) ) ;
#2282=ORIENTED_EDGE ( 'NONE', *, *, #3709, .T. ) ;
#2289=CARTESIAN_POINT ( 'NONE',  ( -3.749999999999999556, -3.750000000000000888, 146.2500000000000000 ) ) ;
#2291=ORIENTED_EDGE ( 'NONE', *, *, #828, .T. ) ;
#2307=FACE_OUTER_BOUND ( 'NONE', #2955, .T. ) ;
#2313=ORIENTED_EDGE ( 'NONE', *, *, #2529, .T. ) ;
#2320=AXIS2_PLACEMENT_3D ( 'NONE', #1417, #2836, #3103 ) ;
#2337=ORIENTED_EDGE ( 'NONE', *, *, #259, .F. ) ;
#2368=VERTEX_POINT ( 'NONE', #4621 ) ;
#2378=CYLINDRICAL_SURFACE ( 'NONE', #1444, 14.28750000000000142 ) ;
#2399=VECTOR ( 'NONE', #595, 1000.000000000000000 ) ;
#2420=SHAPE_REPRESENTATION_RELATIONSHIP ( 'NONE' , 'NONE' ,  #2796, #3970 ) ;
#2455=LINE ( 'NONE', #4562, #3765 ) ;
#2456=ORIENTED_EDGE ( 'NONE', *, *, #3194, .F. ) ;
#2468=PRODUCT_CONTEXT ( 'NONE', #1297, 'mechanical' ) ;
#2473=CARTESIAN_POINT ( 'NONE',  ( 3.750000000000000000, 3.750000000000000000, 146.2500000000000000 ) ) ;
#2484=PLANE ( 'NONE',  #4540 ) ;
#2496=DIRECTION ( 'NONE',  ( -0.000000000000000000, -0.000000000000000000, 1.000000000000000000 ) ) ;
#2507=ORIENTED_EDGE ( 'NONE', *, *, #547, .T. ) ;
#2513=CARTESIAN_POINT ( 'NONE',  ( 3.749999999999999556, 3.750000000000000000, 18.74999999999999645 ) ) ;
#2519=ADVANCED_FACE ( 'NONE', ( #65 ), #43, .F. ) ;
#2523=VECTOR ( 'NONE', #2746, 1000.000000000000000 ) ;
#2529=EDGE_CURVE ( 'NONE', #2975, #1428, #1028, .T. ) ;
#2535=EDGE_LOOP ( 'NONE', ( #2507, #1456, #3541, #4309 ) ) ;
#2549=LINE ( 'NONE', #3993, #154 ) ;
#2554=ORIENTED_EDGE ( 'NONE', *, *, #448, .F. ) ;
#2577=DIRECTION ( 'NONE',  ( 0.000000000000000000, 0.000000000000000000, -1.000000000000000000 ) ) ;
#2582=ORIENTED_EDGE ( 'NONE', *, *, #792, .T. ) ;
#2597=DIRECTION ( 'NONE',  ( 1.000000000000000000, 0.000000000000000000, 0.000000000000000000 ) ) ;
#2603=FACE_OUTER_BOUND ( 'NONE', #2213, .T. ) ;
#2610=LINE ( 'NONE', #4098, #3165 ) ;
#2642=VERTEX_POINT ( 'NONE', #4109 ) ;
#2643=VECTOR ( 'NONE', #112, 1000.000000000000000 ) ;
#2649=VECTOR ( 'NONE', #266, 1000.000000000000000 ) ;
#2658=CARTESIAN_POINT ( 'NONE',  ( -3.750000000000000888, -3.750000000000000000, 3.749999999999995559 ) ) ;
#2660=EDGE_LOOP ( 'NONE', ( #3577, #4016, #1959, #3829 ) ) ;
#2686=CARTESIAN_POINT ( 'NONE',  ( -9.549434556529077899E-17, 3.750000000000000000, 18.74999999999999645 ) ) ;
#2688=VERTEX_POINT ( 'NONE', #3409 ) ;
#2693=CARTESIAN_POINT ( 'NONE',  ( 3.750000000000000000, 3.750000000000000000, 146.2500000000000000 ) ) ;
#2706=VECTOR ( 'NONE', #2271, 1000.000000000000000 ) ;
#2709=DIRECTION ( 'NONE',  ( 1.000000000000000000, -0.000000000000000000, -0.000000000000000000 ) ) ;
#2743=PLANE ( 'NONE',  #283 ) ;
#2746=DIRECTION ( 'NONE',  ( 1.000000000000000000, -0.000000000000000000, -0.000000000000000000 ) ) ;
#2754=CARTESIAN_POINT ( 'NONE',  ( 3.749999999999999556, -3.750000000000000888, 3.749999999999995559 ) ) ;
#2758=FACE_OUTER_BOUND ( 'NONE', #2660, .T. ) ;
#2763=ORIENTED_EDGE ( 'NONE', *, *, #401, .F. ) ;
#2771=EDGE_LOOP ( 'NONE', ( #4181, #494, #630, #701 ) ) ;
#2796=SHAPE_REPRESENTATION ( 'Part 136_Varsay\X2\0131\X0\lan', ( #4483 ), #4552 ) ;
#2836=DIRECTION ( 'NONE',  ( -1.000000000000000000, -8.673617379884035472E-17, 0.000000000000000000 ) ) ;
#2840=EDGE_CURVE ( 'NONE', #2642, #4262, #4166, .T. ) ;
#2888=LINE ( 'NONE', #3183, #4583 ) ;
#2912=VECTOR ( 'NONE', #4606, 1000.000000000000000 ) ;
#2955=EDGE_LOOP ( 'NONE', ( #171, #4547, #77, #1358 ) ) ;
#2975=VERTEX_POINT ( 'NONE', #333 ) ;
#3012=DIRECTION ( 'NONE',  ( -0.000000000000000000, -0.000000000000000000, -1.000000000000000000 ) ) ;
#3020=ADVANCED_FACE ( 'NONE', ( #455 ), #2484, .F. ) ;
#3021=COLOUR_RGB ( '', 0.66274510, 0.83137255, 0.94901961) ;
#3039=ADVANCED_FACE ( 'NONE', ( #700 ), #2139, .F. ) ;
#3067=VECTOR ( 'NONE', #2017, 1000.000000000000000 ) ;
#3087=CARTESIAN_POINT ( 'NONE',  ( 3.750000000000000888, -3.750000000000000000, 146.2500000000000000 ) ) ;
#3091=CARTESIAN_POINT ( 'NONE',  ( 3.750000000000000888, -3.750000000000000000, 146.2500000000000000 ) ) ;
#3103=DIRECTION ( 'NONE',  ( 8.673617379884035472E-17, -1.000000000000000000, 0.000000000000000000 ) ) ;
#3117=ORIENTED_EDGE ( 'NONE', *, *, #894, .T. ) ;
#3124=CARTESIAN_POINT ( 'NONE',  ( -3.750000000000000000, 3.750000000000000000, 3.749999999999995559 ) ) ;
#3125=ORIENTED_EDGE ( 'NONE', *, *, #4281, .T. ) ;
#3144=PLANE ( 'NONE',  #311 ) ;
#3165=VECTOR ( 'NONE', #1566, 1000.000000000000000 ) ;
#3183=CARTESIAN_POINT ( 'NONE',  ( -3.750000000000000888, -3.750000000000000000, 18.74999999999999645 ) ) ;
#3194=EDGE_CURVE ( 'NONE', #1870, #2688, #4297, .T. ) ;
#3203=ORIENTED_EDGE ( 'NONE', *, *, #1316, .F. ) ;
#3222=EDGE_CURVE ( 'NONE', #4262, #3792, #1079, .T. ) ;
#3226=VECTOR ( 'NONE', #1367, 1000.000000000000000 ) ;
#3228=ORIENTED_EDGE ( 'NONE', *, *, #59, .T. ) ;
#3232=DIRECTION ( 'NONE',  ( -0.000000000000000000, -1.000000000000000000, -0.000000000000000000 ) ) ;
#3242=CARTESIAN_POINT ( 'NONE',  ( 3.749999999999999556, -3.750000000000000888, 3.749999999999995559 ) ) ;
#3250=AXIS2_PLACEMENT_3D ( 'NONE', #4042, #3665, #817 ) ;
#3253=EDGE_CURVE ( 'NONE', #3887, #4134, #1481, .T. ) ;
#3268=FACE_OUTER_BOUND ( 'NONE', #2193, .T. ) ;
#3279=EDGE_CURVE ( 'NONE', #744, #4332, #384, .T. ) ;
#3292=CARTESIAN_POINT ( 'NONE',  ( -9.549434556529077899E-17, -3.249382362871961689E-18, 131.2499999999999716 ) ) ;
#3312=VERTEX_POINT ( 'NONE', #1745 ) ;
#3318=VECTOR ( 'NONE', #1614, 1000.000000000000000 ) ;
#3332=DIRECTION ( 'NONE',  ( 0.000000000000000000, 0.000000000000000000, -1.000000000000000000 ) ) ;
#3338=ADVANCED_FACE ( 'NONE', ( #2023 ), #3144, .F. ) ;
#3378=DIRECTION ( 'NONE',  ( 1.000000000000000000, -8.673617379884035472E-17, 0.000000000000000000 ) ) ;
#3388=ORIENTED_EDGE ( 'NONE', *, *, #1589, .F. ) ;
#3392=LINE ( 'NONE', #170, #3318 ) ;
#3407=DIRECTION ( 'NONE',  ( 0.000000000000000000, -0.000000000000000000, -1.000000000000000000 ) ) ;
#3409=CARTESIAN_POINT ( 'NONE',  ( 3.750000000000000000, 3.750000000000000000, 146.2500000000000000 ) ) ;
#3414=VECTOR ( 'NONE', #3916, 1000.000000000000000 ) ;
#3422=DIRECTION ( 'NONE',  ( -1.000000000000000000, 0.000000000000000000, 0.000000000000000000 ) ) ;
#3433=VECTOR ( 'NONE', #1344, 1000.000000000000000 ) ;
#3434=DIRECTION ( 'NONE',  ( 0.000000000000000000, 0.000000000000000000, 1.000000000000000000 ) ) ;
#3469=ADVANCED_FACE ( 'NONE', ( #2307 ), #4104, .F. ) ;
#3473=FILL_AREA_STYLE_COLOUR ( '', #3021 ) ;
#3474=ORIENTED_EDGE ( 'NONE', *, *, #259, .T. ) ;
#3481=LINE ( 'NONE', #4177, #3226 ) ;
#3497=( LENGTH_UNIT ( ) NAMED_UNIT ( * ) SI_UNIT ( .MILLI., .METRE. ) );
#3508=PRODUCT_DEFINITION_SHAPE ( 'NONE', 'NONE',  #14 ) ;
#3514=EDGE_LOOP ( 'NONE', ( #4264, #1774, #3388, #685 ) ) ;
#3527=LINE ( 'NONE', #326, #1687 ) ;
#3534=ORIENTED_EDGE ( 'NONE', *, *, #1129, .T. ) ;
#3541=ORIENTED_EDGE ( 'NONE', *, *, #3253, .F. ) ;
#3551=CARTESIAN_POINT ( 'NONE',  ( -9.549434556529077899E-17, -3.249382362871961689E-18, 18.74999999999999645 ) ) ;
#3558=AXIS2_PLACEMENT_3D ( 'NONE', #771, #353, #1798 ) ;
#3566=EDGE_CURVE ( 'NONE', #44, #2368, #3795, .T. ) ;
#3577=ORIENTED_EDGE ( 'NONE', *, *, #828, .F. ) ;
#3601=DIRECTION ( 'NONE',  ( -8.673617379884035472E-17, 1.000000000000000000, 0.000000000000000000 ) ) ;
#3619=CARTESIAN_POINT ( 'NONE',  ( -9.549434556529077899E-17, 3.750000000000000000, 3.749999999999995559 ) ) ;
#3634=CARTESIAN_POINT ( 'NONE',  ( 3.750000000000000000, 3.750000000000000000, 131.2499999999999716 ) ) ;
#3651=EDGE_CURVE ( 'NONE', #4134, #1870, #1295, .T. ) ;
#3665=DIRECTION ( 'NONE',  ( 0.000000000000000000, 0.000000000000000000, 1.000000000000000000 ) ) ;
#3683=DIRECTION ( 'NONE',  ( 0.000000000000000000, 0.000000000000000000, 1.000000000000000000 ) ) ;
#3687=AXIS2_PLACEMENT_3D ( 'NONE', #1944, #3012, #3422 ) ;
#3688=LINE ( 'NONE', #469, #2643 ) ;
#3690=ORIENTED_EDGE ( 'NONE', *, *, #303, .F. ) ;
#3704=DIRECTION ( 'NONE',  ( 1.000000000000000000, 0.000000000000000000, 0.000000000000000000 ) ) ;
#3706=DIRECTION ( 'NONE',  ( 0.000000000000000000, -1.000000000000000000, 0.000000000000000000 ) ) ;
#3709=EDGE_CURVE ( 'NONE', #4134, #3312, #571, .T. ) ;
#3716=LINE ( 'NONE', #1192, #3751 ) ;
#3747=CYLINDRICAL_SURFACE ( 'NONE', #3687, 14.28750000000000142 ) ;
#3751=VECTOR ( 'NONE', #492, 1000.000000000000000 ) ;
#3752=CARTESIAN_POINT ( 'NONE',  ( 0.000000000000000000, 0.000000000000000000, 0.000000000000000000 ) ) ;
#3761=CIRCLE ( 'NONE', #1747, 14.28750000000000142 ) ;
#3765=VECTOR ( 'NONE', #2112, 1000.000000000000000 ) ;
#3773=UNCERTAINTY_MEASURE_WITH_UNIT (LENGTH_MEASURE( 1.000000000000000082E-05 ), #3497, 'distance_accuracy_value', 'NONE');
#3791=ORIENTED_EDGE ( 'NONE', *, *, #1316, .T. ) ;
#3792=VERTEX_POINT ( 'NONE', #2513 ) ;
#3795=LINE ( 'NONE', #2754, #3892 ) ;
#3814=ORIENTED_EDGE ( 'NONE', *, *, #4429, .T. ) ;
#3818=CARTESIAN_POINT ( 'NONE',  ( -3.749999999999999556, -3.750000000000000888, 146.2500000000000000 ) ) ;
#3824=DIRECTION ( 'NONE',  ( 8.673617379884035472E-17, 1.000000000000000000, 0.000000000000000000 ) ) ;
#3828=CARTESIAN_POINT ( 'NONE',  ( -14.28750000000000142, -3.249382362871961689E-18, 18.74999999999999645 ) ) ;
#3829=ORIENTED_EDGE ( 'NONE', *, *, #1376, .T. ) ;
#3855=ORIENTED_EDGE ( 'NONE', *, *, #2529, .F. ) ;
#3858=SURFACE_STYLE_FILL_AREA ( #4596 ) ;
#3887=VERTEX_POINT ( 'NONE', #1664 ) ;
#3892=VECTOR ( 'NONE', #1363, 1000.000000000000000 ) ;
#3916=DIRECTION ( 'NONE',  ( -8.673617379884035472E-17, 1.000000000000000000, -0.000000000000000000 ) ) ;
#3970=ADVANCED_BREP_SHAPE_REPRESENTATION ( '', ( #275, #4483 ), #4552 ) ;
#3972=CARTESIAN_POINT ( 'NONE',  ( -3.749999999999999556, -3.750000000000000888, 146.2500000000000000 ) ) ;
#3985=ADVANCED_FACE ( 'NONE', ( #4232 ), #2743, .F. ) ;
#3993=CARTESIAN_POINT ( 'NONE',  ( 14.28750000000000142, 1.746464731918909201E-15, 131.2499999999999716 ) ) ;
#4013=DIRECTION ( 'NONE',  ( 0.000000000000000000, 0.000000000000000000, 1.000000000000000000 ) ) ;
#4016=ORIENTED_EDGE ( 'NONE', *, *, #792, .F. ) ;
#4036=DIRECTION ( 'NONE',  ( 8.673617379884035472E-17, 1.000000000000000000, -0.000000000000000000 ) ) ;
#4042=CARTESIAN_POINT ( 'NONE',  ( -9.549434556529077899E-17, -3.249382362871961689E-18, 18.74999999999999645 ) ) ;
#4080=( GEOMETRIC_REPRESENTATION_CONTEXT ( 3 ) GLOBAL_UNCERTAINTY_ASSIGNED_CONTEXT ( ( #199 ) ) GLOBAL_UNIT_ASSIGNED_CONTEXT ( ( #312, #2059, #1017 ) ) REPRESENTATION_CONTEXT ( 'NONE', 'WORKASPACE' ) );
#4090=VERTEX_POINT ( 'NONE', #1514 ) ;
#4098=CARTESIAN_POINT ( 'NONE',  ( -3.750000000000000888, -3.750000000000000000, 3.749999999999995559 ) ) ;
#4100=ORIENTED_EDGE ( 'NONE', *, *, #1793, .F. ) ;
#4104=PLANE ( 'NONE',  #683 ) ;
#4106=LINE ( 'NONE', #1901, #1810 ) ;
#4109=CARTESIAN_POINT ( 'NONE',  ( -3.750000000000000000, 3.750000000000000000, 3.749999999999995559 ) ) ;
#4134=VERTEX_POINT ( 'NONE', #3972 ) ;
#4166=LINE ( 'NONE', #4210, #2523 ) ;
#4177=CARTESIAN_POINT ( 'NONE',  ( -14.28750000000000142, -3.249382362871961689E-18, 131.2499999999999716 ) ) ;
#4181=ORIENTED_EDGE ( 'NONE', *, *, #1834, .T. ) ;
#4210=CARTESIAN_POINT ( 'NONE',  ( 3.749999999999999556, 3.750000000000000000, 3.749999999999995559 ) ) ;
#4214=SURFACE_SIDE_STYLE ('',( #3858 ) ) ;
#4232=FACE_OUTER_BOUND ( 'NONE', #103, .T. ) ;
#4238=LINE ( 'NONE', #1359, #2649 ) ;
#4245=CARTESIAN_POINT ( 'NONE',  ( -9.549434556529077899E-17, -3.249382362871961689E-18, 131.2499999999999716 ) ) ;
#4246=LINE ( 'NONE', #1677, #2912 ) ;
#4250=CARTESIAN_POINT ( 'NONE',  ( -3.750000000000000888, -3.750000000000000000, 3.749999999999995559 ) ) ;
#4262=VERTEX_POINT ( 'NONE', #890 ) ;
#4264=ORIENTED_EDGE ( 'NONE', *, *, #303, .T. ) ;
#4281=EDGE_CURVE ( 'NONE', #2642, #359, #2109, .T. ) ;
#4297=LINE ( 'NONE', #2473, #3414 ) ;
#4309=ORIENTED_EDGE ( 'NONE', *, *, #1699, .T. ) ;
#4316=SHAPE_DEFINITION_REPRESENTATION ( #3508, #2796 ) ;
#4325=DIRECTION ( 'NONE',  ( 0.000000000000000000, -1.000000000000000000, -0.000000000000000000 ) ) ;
#4331=DIRECTION ( 'NONE',  ( -1.000000000000000000, -8.673617379884035472E-17, 0.000000000000000000 ) ) ;
#4332=VERTEX_POINT ( 'NONE', #1004 ) ;
#4371=PLANE ( 'NONE',  #1583 ) ;
#4372=VECTOR ( 'NONE', #2496, 1000.000000000000000 ) ;
#4373=DIRECTION ( 'NONE',  ( -0.000000000000000000, -0.000000000000000000, -1.000000000000000000 ) ) ;
#4381=EDGE_LOOP ( 'NONE', ( #1404, #1046, #627, #3117 ) ) ;
#4394=LINE ( 'NONE', #1181, #4431 ) ;
#4427=DIRECTION ( 'NONE',  ( -1.000000000000000000, 8.673617379884035472E-17, 0.000000000000000000 ) ) ;
#4429=EDGE_CURVE ( 'NONE', #44, #501, #4585, .T. ) ;
#4431=VECTOR ( 'NONE', #4036, 1000.000000000000000 ) ;
#4440=PLANE ( 'NONE',  #305 ) ;
#4467=ORIENTED_EDGE ( 'NONE', *, *, #2840, .F. ) ;
#4483=AXIS2_PLACEMENT_3D ( 'NONE', #3752, #129, #3704 ) ;
#4490=PLANE ( 'NONE',  #2110 ) ;
#4520=VERTEX_POINT ( 'NONE', #3634 ) ;
#4529=DIRECTION ( 'NONE',  ( -0.000000000000000000, -0.000000000000000000, -1.000000000000000000 ) ) ;
#4530=VERTEX_POINT ( 'NONE', #412 ) ;
#4540=AXIS2_PLACEMENT_3D ( 'NONE', #2162, #3601, #4331 ) ;
#4547=ORIENTED_EDGE ( 'NONE', *, *, #3253, .T. ) ;
#4549=LINE ( 'NONE', #3087, #2057 ) ;
#4552=( GEOMETRIC_REPRESENTATION_CONTEXT ( 3 ) GLOBAL_UNCERTAINTY_ASSIGNED_CONTEXT ( ( #3773 ) ) GLOBAL_UNIT_ASSIGNED_CONTEXT ( ( #3497, #956, #1024 ) ) REPRESENTATION_CONTEXT ( 'NONE', 'WORKASPACE' ) );
#4562=CARTESIAN_POINT ( 'NONE',  ( -3.749999999999999556, 3.750000000000000000, 146.2500000000000000 ) ) ;
#4572=SURFACE_STYLE_USAGE ( .BOTH. , #4214 ) ;
#4583=VECTOR ( 'NONE', #4427, 1000.000000000000000 ) ;
#4584=DIRECTION ( 'NONE',  ( -1.000000000000000000, 8.673617379884035472E-17, 0.000000000000000000 ) ) ;
#4585=LINE ( 'NONE', #298, #3433 ) ;
#4596=FILL_AREA_STYLE ('',( #3473 ) ) ;
#4606=DIRECTION ( 'NONE',  ( -0.000000000000000000, -1.000000000000000000, -0.000000000000000000 ) ) ;
#4613=ORIENTED_EDGE ( 'NONE', *, *, #4429, .F. ) ;
#4621=CARTESIAN_POINT ( 'NONE',  ( 3.749999999999999556, -3.750000000000000888, 18.74999999999999645 ) ) ;
#4632=PLANE ( 'NONE',  #2320 ) ;
#4640=ADVANCED_FACE ( 'NONE', ( #1551 ), #1601, .F. ) ;
ENDSEC;
END-ISO-10303-21;
